ISO-10303-21;
HEADER;
/* Generated by software containing ST-Developer
 * from STEP Tools, Inc. (www.steptools.com) 
 */

FILE_DESCRIPTION(
/* description */ (
'Independent keyed-quill tailstock, native coupled50mm slider andM16x2
 feed screw, conical dead center, bronze sleeves/thrust washers, cross
-pinned handwheel and bolted guide key. Custom center taper; no standa
rd taper compatibility, machine-bed compatibility or load rating assig
ned.'),
/* implementation_level */ '2;1');

FILE_NAME(
/* name */ 'Thrust washer.step',
/* time_stamp */ '2026-11-14T07:17:36-08:00',
/* author */ (''),
/* organization */ (''),
/* preprocessor_version */ 'ST-DEVELOPER v20.2',
/* originating_system */ 'Autodesk Translation Framework v15.17.0.0',
/* authorisation */ '');

FILE_SCHEMA (('AUTOMOTIVE_DESIGN { 1 0 10303 214 3 1 1 }'));
ENDSEC;

DATA;
#10=MECHANICAL_DESIGN_GEOMETRIC_PRESENTATION_REPRESENTATION('',(#166),#289387);
#132=SHAPE_REPRESENTATION_RELATIONSHIP('SRR','None',#289467,#149);
#149=ADVANCED_BREP_SHAPE_REPRESENTATION('',(#183),#289383);
#166=STYLED_ITEM('',(#289550),#183);
#183=MANIFOLD_SOLID_BREP('Body1',#16854);
#265=FACE_BOUND('',#1706,.T.);
#266=FACE_BOUND('',#1708,.T.);
#391=PLANE('',#17745);
#392=PLANE('',#17746);
#975=FACE_OUTER_BOUND('',#1703,.T.);
#976=FACE_OUTER_BOUND('',#1704,.T.);
#977=FACE_OUTER_BOUND('',#1705,.T.);
#978=FACE_OUTER_BOUND('',#1707,.T.);
#1703=EDGE_LOOP('',(#14833,#14834,#14835,#14836));
#1704=EDGE_LOOP('',(#14837,#14838,#14839,#14840));
#1705=EDGE_LOOP('',(#14841));
#1706=EDGE_LOOP('',(#14842));
#1707=EDGE_LOOP('',(#14843));
#1708=EDGE_LOOP('',(#14844));
#1959=CIRCLE('',#17740,6.);
#1960=CIRCLE('',#17741,6.);
#1961=CIRCLE('',#17743,12.);
#1962=CIRCLE('',#17744,12.);
#4470=LINE('',#247338,#5107);
#4471=LINE('',#247344,#5108);
#5107=VECTOR('',#19808,6.);
#5108=VECTOR('',#19815,12.);
#7043=VERTEX_POINT('',#247335);
#7044=VERTEX_POINT('',#247337);
#7045=VERTEX_POINT('',#247341);
#7046=VERTEX_POINT('',#247343);
#9728=EDGE_CURVE('',#7043,#7043,#1959,.T.);
#9729=EDGE_CURVE('',#7043,#7044,#4470,.T.);
#9730=EDGE_CURVE('',#7044,#7044,#1960,.T.);
#9731=EDGE_CURVE('',#7045,#7045,#1961,.T.);
#9732=EDGE_CURVE('',#7045,#7046,#4471,.T.);
#9733=EDGE_CURVE('',#7046,#7046,#1962,.T.);
#14833=ORIENTED_EDGE('',*,*,#9728,.T.);
#14834=ORIENTED_EDGE('',*,*,#9729,.T.);
#14835=ORIENTED_EDGE('',*,*,#9730,.F.);
#14836=ORIENTED_EDGE('',*,*,#9729,.F.);
#14837=ORIENTED_EDGE('',*,*,#9731,.F.);
#14838=ORIENTED_EDGE('',*,*,#9732,.T.);
#14839=ORIENTED_EDGE('',*,*,#9733,.T.);
#14840=ORIENTED_EDGE('',*,*,#9732,.F.);
#14841=ORIENTED_EDGE('',*,*,#9731,.T.);
#14842=ORIENTED_EDGE('',*,*,#9730,.T.);
#14843=ORIENTED_EDGE('',*,*,#9733,.F.);
#14844=ORIENTED_EDGE('',*,*,#9728,.F.);
#16136=CYLINDRICAL_SURFACE('',#17739,6.);
#16137=CYLINDRICAL_SURFACE('',#17742,12.);
#16743=ADVANCED_FACE('',(#975),#16136,.F.);
#16744=ADVANCED_FACE('',(#976),#16137,.T.);
#16745=ADVANCED_FACE('',(#977,#265),#391,.T.);
#16746=ADVANCED_FACE('',(#978,#266),#392,.F.);
#16854=CLOSED_SHELL('',(#16743,#16744,#16745,#16746));
#17738=AXIS2_PLACEMENT_3D('',#247333,#19802,#19803);
#17739=AXIS2_PLACEMENT_3D('',#247334,#19804,#19805);
#17740=AXIS2_PLACEMENT_3D('',#247336,#19806,#19807);
#17741=AXIS2_PLACEMENT_3D('',#247339,#19809,#19810);
#17742=AXIS2_PLACEMENT_3D('',#247340,#19811,#19812);
#17743=AXIS2_PLACEMENT_3D('',#247342,#19813,#19814);
#17744=AXIS2_PLACEMENT_3D('',#247345,#19816,#19817);
#17745=AXIS2_PLACEMENT_3D('',#247346,#19818,#19819);
#17746=AXIS2_PLACEMENT_3D('',#247347,#19820,#19821);
#19802=DIRECTION('axis',(0.,0.,1.));
#19803=DIRECTION('refdir',(1.,0.,0.));
#19804=DIRECTION('center_axis',(0.,0.,1.));
#19805=DIRECTION('ref_axis',(1.,0.,0.));
#19806=DIRECTION('center_axis',(0.,0.,-1.));
#19807=DIRECTION('ref_axis',(1.,0.,0.));
#19808=DIRECTION('',(0.,0.,1.));
#19809=DIRECTION('center_axis',(0.,0.,-1.));
#19810=DIRECTION('ref_axis',(1.,0.,0.));
#19811=DIRECTION('center_axis',(0.,0.,1.));
#19812=DIRECTION('ref_axis',(1.,0.,0.));
#19813=DIRECTION('center_axis',(0.,0.,1.));
#19814=DIRECTION('ref_axis',(1.,0.,0.));
#19815=DIRECTION('',(0.,0.,-1.));
#19816=DIRECTION('center_axis',(0.,0.,1.));
#19817=DIRECTION('ref_axis',(1.,0.,0.));
#19818=DIRECTION('center_axis',(0.,0.,1.));
#19819=DIRECTION('ref_axis',(1.,0.,0.));
#19820=DIRECTION('center_axis',(0.,0.,1.));
#19821=DIRECTION('ref_axis',(1.,0.,0.));
#247333=CARTESIAN_POINT('',(0.,0.,0.));
#247334=CARTESIAN_POINT('Origin',(0.,0.,0.));
#247335=CARTESIAN_POINT('',(-6.,-7.34788079488412E-16,0.));
#247336=CARTESIAN_POINT('Origin',(0.,0.,0.));
#247337=CARTESIAN_POINT('',(-6.,-7.34788079488412E-16,4.));
#247338=CARTESIAN_POINT('',(-6.,-7.34788079488412E-16,0.));
#247339=CARTESIAN_POINT('Origin',(0.,0.,4.));
#247340=CARTESIAN_POINT('Origin',(0.,0.,0.));
#247341=CARTESIAN_POINT('',(-12.,-1.46957615897682E-15,4.));
#247342=CARTESIAN_POINT('Origin',(0.,0.,4.));
#247343=CARTESIAN_POINT('',(-12.,-1.46957615897682E-15,0.));
#247344=CARTESIAN_POINT('',(-12.,-1.46957615897682E-15,0.));
#247345=CARTESIAN_POINT('Origin',(0.,0.,0.));
#247346=CARTESIAN_POINT('Origin',(0.,0.,4.));
#247347=CARTESIAN_POINT('Origin',(0.,0.,0.));
#289364=UNCERTAINTY_MEASURE_WITH_UNIT(LENGTH_MEASURE(0.01),#289388,
'DISTANCE_ACCURACY_VALUE',
'Maximum model space distance between geometric entities at asserted c
onnectivities');
#289368=UNCERTAINTY_MEASURE_WITH_UNIT(LENGTH_MEASURE(0.01),#289388,
'DISTANCE_ACCURACY_VALUE',
'Maximum model space distance between geometric entities at asserted c
onnectivities');
#289383=(
GEOMETRIC_REPRESENTATION_CONTEXT(3)
GLOBAL_UNCERTAINTY_ASSIGNED_CONTEXT((#289364))
GLOBAL_UNIT_ASSIGNED_CONTEXT((#289388,#289390,#289391))
REPRESENTATION_CONTEXT('','3D')
);
#289387=(
GEOMETRIC_REPRESENTATION_CONTEXT(3)
GLOBAL_UNCERTAINTY_ASSIGNED_CONTEXT((#289368))
GLOBAL_UNIT_ASSIGNED_CONTEXT((#289388,#289390,#289391))
REPRESENTATION_CONTEXT('','3D')
);
#289388=(
LENGTH_UNIT()
NAMED_UNIT(*)
SI_UNIT(.MILLI.,.METRE.)
);
#289390=(
NAMED_UNIT(*)
PLANE_ANGLE_UNIT()
SI_UNIT($,.RADIAN.)
);
#289391=(
NAMED_UNIT(*)
SI_UNIT($,.STERADIAN.)
SOLID_ANGLE_UNIT()
);
#289406=SHAPE_DEFINITION_REPRESENTATION(#289424,#289467);
#289424=PRODUCT_DEFINITION_SHAPE('',$,#289486);
#289467=SHAPE_REPRESENTATION('',(#17738),#289383);
#289471=PRODUCT_DEFINITION_CONTEXT('part definition',#289527,'design');
#289486=PRODUCT_DEFINITION('Thrust washer','Thrust washer',#289504,#289471);
#289504=PRODUCT_DEFINITION_FORMATION('',$,#289543);
#289527=APPLICATION_CONTEXT(
'Core Data for Automotive Mechanical Design Process');
#289528=PRODUCT_CONTEXT('part definition',#289527,'mechanical');
#289543=PRODUCT('Thrust washer','Thrust washer',$,(#289528));
#289550=PRESENTATION_STYLE_ASSIGNMENT((#289557));
#289557=SURFACE_STYLE_USAGE(.BOTH.,#289564);
#289564=SURFACE_SIDE_STYLE('',(#289571));
#289571=SURFACE_STYLE_FILL_AREA(#289578);
#289578=FILL_AREA_STYLE('Opaque(185,192,202)',(#289585));
#289585=FILL_AREA_STYLE_COLOUR('Opaque(185,192,202)',#289592);
#289592=COLOUR_RGB('Opaque(185,192,202)',0.725490196078431,0.752941176470588,
0.792156862745098);
ENDSEC;
END-ISO-10303-21;
